ISO-10303-21;
HEADER;
/* Generated by software containing ST-Developer
 * from STEP Tools, Inc. (www.steptools.com) 
 */

FILE_DESCRIPTION(
/* description */ ('STEP AP214'),
/* implementation_level */ '2;1');

FILE_NAME(
/* name */ 'Ball Screw Spacer 2.step',
/* time_stamp */ '2026-11-15T14:55:55-08:00',
/* author */ (''),
/* organization */ (''),
/* preprocessor_version */ 'ST-DEVELOPER v20.2',
/* originating_system */ 'Autodesk Translation Framework v15.17.0.0',
/* authorisation */ '');

FILE_SCHEMA (('AUTOMOTIVE_DESIGN { 1 0 10303 214 3 1 1 }'));
ENDSEC;

DATA;
#10=MECHANICAL_DESIGN_GEOMETRIC_PRESENTATION_REPRESENTATION('',(#937),#57079);
#877=SHAPE_REPRESENTATION_RELATIONSHIP('SRR','None',#57263,#906);
#906=ADVANCED_BREP_SHAPE_REPRESENTATION('',(#974),#57055);
#937=STYLED_ITEM('',(#57444),#974);
#974=MANIFOLD_SOLID_BREP('Body1',#24537);
#1101=FACE_BOUND('',#3925,.T.);
#1102=FACE_BOUND('',#3926,.T.);
#1103=FACE_BOUND('',#3927,.T.);
#1104=FACE_BOUND('',#3928,.T.);
#1105=FACE_BOUND('',#3934,.T.);
#1106=FACE_BOUND('',#3935,.T.);
#1107=FACE_BOUND('',#3936,.T.);
#1108=FACE_BOUND('',#3937,.T.);
#1512=PLANE('',#25410);
#1513=PLANE('',#25411);
#1514=PLANE('',#25412);
#1515=PLANE('',#25413);
#1516=PLANE('',#25414);
#1517=PLANE('',#25415);
#1518=PLANE('',#25416);
#1519=PLANE('',#25417);
#1520=PLANE('',#25418);
#1521=PLANE('',#25419);
#1522=PLANE('',#25420);
#1523=PLANE('',#25421);
#2438=FACE_OUTER_BOUND('',#3914,.T.);
#2439=FACE_OUTER_BOUND('',#3915,.T.);
#2440=FACE_OUTER_BOUND('',#3916,.T.);
#2441=FACE_OUTER_BOUND('',#3917,.T.);
#2442=FACE_OUTER_BOUND('',#3918,.T.);
#2443=FACE_OUTER_BOUND('',#3919,.T.);
#2444=FACE_OUTER_BOUND('',#3920,.T.);
#2445=FACE_OUTER_BOUND('',#3921,.T.);
#2446=FACE_OUTER_BOUND('',#3922,.T.);
#2447=FACE_OUTER_BOUND('',#3923,.T.);
#2448=FACE_OUTER_BOUND('',#3924,.T.);
#2449=FACE_OUTER_BOUND('',#3929,.T.);
#2450=FACE_OUTER_BOUND('',#3930,.T.);
#2451=FACE_OUTER_BOUND('',#3931,.T.);
#2452=FACE_OUTER_BOUND('',#3932,.T.);
#2453=FACE_OUTER_BOUND('',#3933,.T.);
#3914=EDGE_LOOP('',(#17180,#17181,#17182,#17183));
#3915=EDGE_LOOP('',(#17184,#17185,#17186,#17187));
#3916=EDGE_LOOP('',(#17188,#17189,#17190,#17191));
#3917=EDGE_LOOP('',(#17192,#17193,#17194,#17195));
#3918=EDGE_LOOP('',(#17196,#17197,#17198,#17199));
#3919=EDGE_LOOP('',(#17200,#17201,#17202,#17203,#17204,#17205));
#3920=EDGE_LOOP('',(#17206,#17207,#17208,#17209,#17210,#17211));
#3921=EDGE_LOOP('',(#17212,#17213,#17214,#17215,#17216,#17217));
#3922=EDGE_LOOP('',(#17218,#17219,#17220,#17221,#17222,#17223));
#3923=EDGE_LOOP('',(#17224,#17225,#17226,#17227));
#3924=EDGE_LOOP('',(#17228,#17229,#17230,#17231));
#3925=EDGE_LOOP('',(#17232));
#3926=EDGE_LOOP('',(#17233));
#3927=EDGE_LOOP('',(#17234));
#3928=EDGE_LOOP('',(#17235));
#3929=EDGE_LOOP('',(#17236,#17237,#17238,#17239));
#3930=EDGE_LOOP('',(#17240,#17241,#17242,#17243));
#3931=EDGE_LOOP('',(#17244,#17245,#17246,#17247));
#3932=EDGE_LOOP('',(#17248,#17249,#17250,#17251));
#3933=EDGE_LOOP('',(#17252,#17253,#17254,#17255,#17256,#17257,#17258,#17259));
#3934=EDGE_LOOP('',(#17260));
#3935=EDGE_LOOP('',(#17261));
#3936=EDGE_LOOP('',(#17262));
#3937=EDGE_LOOP('',(#17263));
#5655=LINE('',#36209,#7622);
#5656=LINE('',#36215,#7623);
#5657=LINE('',#36221,#7624);
#5658=LINE('',#36227,#7625);
#5659=LINE('',#36232,#7626);
#5660=LINE('',#36234,#7627);
#5661=LINE('',#36236,#7628);
#5662=LINE('',#36237,#7629);
#5663=LINE('',#36240,#7630);
#5664=LINE('',#36242,#7631);
#5665=LINE('',#36244,#7632);
#5666=LINE('',#36246,#7633);
#5667=LINE('',#36247,#7634);
#5668=LINE('',#36251,#7635);
#5669=LINE('',#36252,#7636);
#5670=LINE('',#36254,#7637);
#5671=LINE('',#36255,#7638);
#5672=LINE('',#36259,#7639);
#5673=LINE('',#36261,#7640);
#5674=LINE('',#36262,#7641);
#5675=LINE('',#36264,#7642);
#5676=LINE('',#36265,#7643);
#5677=LINE('',#36268,#7644);
#5678=LINE('',#36270,#7645);
#5679=LINE('',#36271,#7646);
#5680=LINE('',#36272,#7647);
#5681=LINE('',#36275,#7648);
#5682=LINE('',#36276,#7649);
#5683=LINE('',#36280,#7650);
#5684=LINE('',#36281,#7651);
#5685=LINE('',#36283,#7652);
#5686=LINE('',#36286,#7653);
#5687=LINE('',#36287,#7654);
#5688=LINE('',#36289,#7655);
#7622=VECTOR('',#28915,3.);
#7623=VECTOR('',#28922,3.);
#7624=VECTOR('',#28929,4.25000000000001);
#7625=VECTOR('',#28936,4.25000000000001);
#7626=VECTOR('',#28941,1000.);
#7627=VECTOR('',#28942,1000.);
#7628=VECTOR('',#28943,1000.);
#7629=VECTOR('',#28944,1000.);
#7630=VECTOR('',#28947,1000.);
#7631=VECTOR('',#28948,1000.);
#7632=VECTOR('',#28949,1000.);
#7633=VECTOR('',#28950,1000.);
#7634=VECTOR('',#28951,1000.);
#7635=VECTOR('',#28954,1000.);
#7636=VECTOR('',#28955,1000.);
#7637=VECTOR('',#28956,1000.);
#7638=VECTOR('',#28957,1000.);
#7639=VECTOR('',#28960,1000.);
#7640=VECTOR('',#28961,1000.);
#7641=VECTOR('',#28962,1000.);
#7642=VECTOR('',#28963,1000.);
#7643=VECTOR('',#28964,1000.);
#7644=VECTOR('',#28967,1000.);
#7645=VECTOR('',#28968,1000.);
#7646=VECTOR('',#28969,1000.);
#7647=VECTOR('',#28970,1000.);
#7648=VECTOR('',#28973,1000.);
#7649=VECTOR('',#28974,1000.);
#7650=VECTOR('',#28979,1000.);
#7651=VECTOR('',#28980,1000.);
#7652=VECTOR('',#28983,1000.);
#7653=VECTOR('',#28986,1000.);
#7654=VECTOR('',#28987,1000.);
#7655=VECTOR('',#28990,1000.);
#9398=CIRCLE('',#25399,3.);
#9399=CIRCLE('',#25400,3.);
#9400=CIRCLE('',#25402,3.);
#9401=CIRCLE('',#25403,3.);
#9402=CIRCLE('',#25405,4.25000000000001);
#9403=CIRCLE('',#25406,4.25000000000001);
#9404=CIRCLE('',#25408,4.25000000000001);
#9405=CIRCLE('',#25409,4.25000000000001);
#10691=VERTEX_POINT('',#36206);
#10692=VERTEX_POINT('',#36208);
#10693=VERTEX_POINT('',#36212);
#10694=VERTEX_POINT('',#36214);
#10695=VERTEX_POINT('',#36218);
#10696=VERTEX_POINT('',#36220);
#10697=VERTEX_POINT('',#36224);
#10698=VERTEX_POINT('',#36226);
#10699=VERTEX_POINT('',#36230);
#10700=VERTEX_POINT('',#36231);
#10701=VERTEX_POINT('',#36233);
#10702=VERTEX_POINT('',#36235);
#10703=VERTEX_POINT('',#36239);
#10704=VERTEX_POINT('',#36241);
#10705=VERTEX_POINT('',#36243);
#10706=VERTEX_POINT('',#36245);
#10707=VERTEX_POINT('',#36249);
#10708=VERTEX_POINT('',#36250);
#10709=VERTEX_POINT('',#36253);
#10710=VERTEX_POINT('',#36257);
#10711=VERTEX_POINT('',#36258);
#10712=VERTEX_POINT('',#36260);
#10713=VERTEX_POINT('',#36263);
#10714=VERTEX_POINT('',#36267);
#10715=VERTEX_POINT('',#36269);
#10716=VERTEX_POINT('',#36274);
#10717=VERTEX_POINT('',#36279);
#10718=VERTEX_POINT('',#36285);
#13135=EDGE_CURVE('',#10691,#10691,#9398,.T.);
#13136=EDGE_CURVE('',#10691,#10692,#5655,.T.);
#13137=EDGE_CURVE('',#10692,#10692,#9399,.T.);
#13138=EDGE_CURVE('',#10693,#10693,#9400,.T.);
#13139=EDGE_CURVE('',#10693,#10694,#5656,.T.);
#13140=EDGE_CURVE('',#10694,#10694,#9401,.T.);
#13141=EDGE_CURVE('',#10695,#10695,#9402,.T.);
#13142=EDGE_CURVE('',#10695,#10696,#5657,.T.);
#13143=EDGE_CURVE('',#10696,#10696,#9403,.T.);
#13144=EDGE_CURVE('',#10697,#10697,#9404,.T.);
#13145=EDGE_CURVE('',#10697,#10698,#5658,.T.);
#13146=EDGE_CURVE('',#10698,#10698,#9405,.T.);
#13147=EDGE_CURVE('',#10699,#10700,#5659,.T.);
#13148=EDGE_CURVE('',#10701,#10699,#5660,.T.);
#13149=EDGE_CURVE('',#10701,#10702,#5661,.T.);
#13150=EDGE_CURVE('',#10702,#10700,#5662,.T.);
#13151=EDGE_CURVE('',#10703,#10701,#5663,.T.);
#13152=EDGE_CURVE('',#10704,#10703,#5664,.T.);
#13153=EDGE_CURVE('',#10704,#10705,#5665,.T.);
#13154=EDGE_CURVE('',#10705,#10706,#5666,.T.);
#13155=EDGE_CURVE('',#10702,#10706,#5667,.T.);
#13156=EDGE_CURVE('',#10707,#10708,#5668,.T.);
#13157=EDGE_CURVE('',#10707,#10700,#5669,.T.);
#13158=EDGE_CURVE('',#10706,#10709,#5670,.T.);
#13159=EDGE_CURVE('',#10708,#10709,#5671,.T.);
#13160=EDGE_CURVE('',#10710,#10711,#5672,.T.);
#13161=EDGE_CURVE('',#10712,#10710,#5673,.T.);
#13162=EDGE_CURVE('',#10708,#10712,#5674,.T.);
#13163=EDGE_CURVE('',#10709,#10713,#5675,.T.);
#13164=EDGE_CURVE('',#10711,#10713,#5676,.T.);
#13165=EDGE_CURVE('',#10714,#10704,#5677,.T.);
#13166=EDGE_CURVE('',#10714,#10715,#5678,.T.);
#13167=EDGE_CURVE('',#10711,#10715,#5679,.T.);
#13168=EDGE_CURVE('',#10713,#10705,#5680,.T.);
#13169=EDGE_CURVE('',#10716,#10715,#5681,.T.);
#13170=EDGE_CURVE('',#10710,#10716,#5682,.T.);
#13171=EDGE_CURVE('',#10717,#10707,#5683,.T.);
#13172=EDGE_CURVE('',#10717,#10699,#5684,.T.);
#13173=EDGE_CURVE('',#10703,#10717,#5685,.T.);
#13174=EDGE_CURVE('',#10718,#10714,#5686,.T.);
#13175=EDGE_CURVE('',#10718,#10716,#5687,.T.);
#13176=EDGE_CURVE('',#10712,#10718,#5688,.T.);
#17180=ORIENTED_EDGE('',*,*,#13135,.F.);
#17181=ORIENTED_EDGE('',*,*,#13136,.T.);
#17182=ORIENTED_EDGE('',*,*,#13137,.T.);
#17183=ORIENTED_EDGE('',*,*,#13136,.F.);
#17184=ORIENTED_EDGE('',*,*,#13138,.F.);
#17185=ORIENTED_EDGE('',*,*,#13139,.T.);
#17186=ORIENTED_EDGE('',*,*,#13140,.T.);
#17187=ORIENTED_EDGE('',*,*,#13139,.F.);
#17188=ORIENTED_EDGE('',*,*,#13141,.F.);
#17189=ORIENTED_EDGE('',*,*,#13142,.T.);
#17190=ORIENTED_EDGE('',*,*,#13143,.T.);
#17191=ORIENTED_EDGE('',*,*,#13142,.F.);
#17192=ORIENTED_EDGE('',*,*,#13144,.F.);
#17193=ORIENTED_EDGE('',*,*,#13145,.T.);
#17194=ORIENTED_EDGE('',*,*,#13146,.T.);
#17195=ORIENTED_EDGE('',*,*,#13145,.F.);
#17196=ORIENTED_EDGE('',*,*,#13147,.F.);
#17197=ORIENTED_EDGE('',*,*,#13148,.F.);
#17198=ORIENTED_EDGE('',*,*,#13149,.T.);
#17199=ORIENTED_EDGE('',*,*,#13150,.T.);
#17200=ORIENTED_EDGE('',*,*,#13149,.F.);
#17201=ORIENTED_EDGE('',*,*,#13151,.F.);
#17202=ORIENTED_EDGE('',*,*,#13152,.F.);
#17203=ORIENTED_EDGE('',*,*,#13153,.T.);
#17204=ORIENTED_EDGE('',*,*,#13154,.T.);
#17205=ORIENTED_EDGE('',*,*,#13155,.F.);
#17206=ORIENTED_EDGE('',*,*,#13156,.F.);
#17207=ORIENTED_EDGE('',*,*,#13157,.T.);
#17208=ORIENTED_EDGE('',*,*,#13150,.F.);
#17209=ORIENTED_EDGE('',*,*,#13155,.T.);
#17210=ORIENTED_EDGE('',*,*,#13158,.T.);
#17211=ORIENTED_EDGE('',*,*,#13159,.F.);
#17212=ORIENTED_EDGE('',*,*,#13160,.F.);
#17213=ORIENTED_EDGE('',*,*,#13161,.F.);
#17214=ORIENTED_EDGE('',*,*,#13162,.F.);
#17215=ORIENTED_EDGE('',*,*,#13159,.T.);
#17216=ORIENTED_EDGE('',*,*,#13163,.T.);
#17217=ORIENTED_EDGE('',*,*,#13164,.F.);
#17218=ORIENTED_EDGE('',*,*,#13165,.F.);
#17219=ORIENTED_EDGE('',*,*,#13166,.T.);
#17220=ORIENTED_EDGE('',*,*,#13167,.F.);
#17221=ORIENTED_EDGE('',*,*,#13164,.T.);
#17222=ORIENTED_EDGE('',*,*,#13168,.T.);
#17223=ORIENTED_EDGE('',*,*,#13153,.F.);
#17224=ORIENTED_EDGE('',*,*,#13169,.F.);
#17225=ORIENTED_EDGE('',*,*,#13170,.F.);
#17226=ORIENTED_EDGE('',*,*,#13160,.T.);
#17227=ORIENTED_EDGE('',*,*,#13167,.T.);
#17228=ORIENTED_EDGE('',*,*,#13154,.F.);
#17229=ORIENTED_EDGE('',*,*,#13168,.F.);
#17230=ORIENTED_EDGE('',*,*,#13163,.F.);
#17231=ORIENTED_EDGE('',*,*,#13158,.F.);
#17232=ORIENTED_EDGE('',*,*,#13135,.T.);
#17233=ORIENTED_EDGE('',*,*,#13138,.T.);
#17234=ORIENTED_EDGE('',*,*,#13141,.T.);
#17235=ORIENTED_EDGE('',*,*,#13144,.T.);
#17236=ORIENTED_EDGE('',*,*,#13147,.T.);
#17237=ORIENTED_EDGE('',*,*,#13157,.F.);
#17238=ORIENTED_EDGE('',*,*,#13171,.F.);
#17239=ORIENTED_EDGE('',*,*,#13172,.T.);
#17240=ORIENTED_EDGE('',*,*,#13148,.T.);
#17241=ORIENTED_EDGE('',*,*,#13172,.F.);
#17242=ORIENTED_EDGE('',*,*,#13173,.F.);
#17243=ORIENTED_EDGE('',*,*,#13151,.T.);
#17244=ORIENTED_EDGE('',*,*,#13169,.T.);
#17245=ORIENTED_EDGE('',*,*,#13166,.F.);
#17246=ORIENTED_EDGE('',*,*,#13174,.F.);
#17247=ORIENTED_EDGE('',*,*,#13175,.T.);
#17248=ORIENTED_EDGE('',*,*,#13170,.T.);
#17249=ORIENTED_EDGE('',*,*,#13175,.F.);
#17250=ORIENTED_EDGE('',*,*,#13176,.F.);
#17251=ORIENTED_EDGE('',*,*,#13161,.T.);
#17252=ORIENTED_EDGE('',*,*,#13162,.T.);
#17253=ORIENTED_EDGE('',*,*,#13176,.T.);
#17254=ORIENTED_EDGE('',*,*,#13174,.T.);
#17255=ORIENTED_EDGE('',*,*,#13165,.T.);
#17256=ORIENTED_EDGE('',*,*,#13152,.T.);
#17257=ORIENTED_EDGE('',*,*,#13173,.T.);
#17258=ORIENTED_EDGE('',*,*,#13171,.T.);
#17259=ORIENTED_EDGE('',*,*,#13156,.T.);
#17260=ORIENTED_EDGE('',*,*,#13137,.F.);
#17261=ORIENTED_EDGE('',*,*,#13140,.F.);
#17262=ORIENTED_EDGE('',*,*,#13143,.F.);
#17263=ORIENTED_EDGE('',*,*,#13146,.F.);
#22822=CYLINDRICAL_SURFACE('',#25398,3.);
#22823=CYLINDRICAL_SURFACE('',#25401,3.);
#22824=CYLINDRICAL_SURFACE('',#25404,4.25000000000001);
#22825=CYLINDRICAL_SURFACE('',#25407,4.25000000000001);
#23430=ADVANCED_FACE('',(#2438),#22822,.F.);
#23431=ADVANCED_FACE('',(#2439),#22823,.F.);
#23432=ADVANCED_FACE('',(#2440),#22824,.F.);
#23433=ADVANCED_FACE('',(#2441),#22825,.F.);
#23434=ADVANCED_FACE('',(#2442),#1512,.T.);
#23435=ADVANCED_FACE('',(#2443),#1513,.F.);
#23436=ADVANCED_FACE('',(#2444),#1514,.F.);
#23437=ADVANCED_FACE('',(#2445),#1515,.F.);
#23438=ADVANCED_FACE('',(#2446),#1516,.F.);
#23439=ADVANCED_FACE('',(#2447),#1517,.T.);
#23440=ADVANCED_FACE('',(#2448,#1101,#1102,#1103,#1104),#1518,.F.);
#23441=ADVANCED_FACE('',(#2449),#1519,.F.);
#23442=ADVANCED_FACE('',(#2450),#1520,.F.);
#23443=ADVANCED_FACE('',(#2451),#1521,.F.);
#23444=ADVANCED_FACE('',(#2452),#1522,.F.);
#23445=ADVANCED_FACE('',(#2453,#1105,#1106,#1107,#1108),#1523,.T.);
#24537=CLOSED_SHELL('',(#23430,#23431,#23432,#23433,#23434,#23435,#23436,
#23437,#23438,#23439,#23440,#23441,#23442,#23443,#23444,#23445));
#25397=AXIS2_PLACEMENT_3D('',#36204,#28909,#28910);
#25398=AXIS2_PLACEMENT_3D('',#36205,#28911,#28912);
#25399=AXIS2_PLACEMENT_3D('',#36207,#28913,#28914);
#25400=AXIS2_PLACEMENT_3D('',#36210,#28916,#28917);
#25401=AXIS2_PLACEMENT_3D('',#36211,#28918,#28919);
#25402=AXIS2_PLACEMENT_3D('',#36213,#28920,#28921);
#25403=AXIS2_PLACEMENT_3D('',#36216,#28923,#28924);
#25404=AXIS2_PLACEMENT_3D('',#36217,#28925,#28926);
#25405=AXIS2_PLACEMENT_3D('',#36219,#28927,#28928);
#25406=AXIS2_PLACEMENT_3D('',#36222,#28930,#28931);
#25407=AXIS2_PLACEMENT_3D('',#36223,#28932,#28933);
#25408=AXIS2_PLACEMENT_3D('',#36225,#28934,#28935);
#25409=AXIS2_PLACEMENT_3D('',#36228,#28937,#28938);
#25410=AXIS2_PLACEMENT_3D('',#36229,#28939,#28940);
#25411=AXIS2_PLACEMENT_3D('',#36238,#28945,#28946);
#25412=AXIS2_PLACEMENT_3D('',#36248,#28952,#28953);
#25413=AXIS2_PLACEMENT_3D('',#36256,#28958,#28959);
#25414=AXIS2_PLACEMENT_3D('',#36266,#28965,#28966);
#25415=AXIS2_PLACEMENT_3D('',#36273,#28971,#28972);
#25416=AXIS2_PLACEMENT_3D('',#36277,#28975,#28976);
#25417=AXIS2_PLACEMENT_3D('',#36278,#28977,#28978);
#25418=AXIS2_PLACEMENT_3D('',#36282,#28981,#28982);
#25419=AXIS2_PLACEMENT_3D('',#36284,#28984,#28985);
#25420=AXIS2_PLACEMENT_3D('',#36288,#28988,#28989);
#25421=AXIS2_PLACEMENT_3D('',#36290,#28991,#28992);
#28909=DIRECTION('axis',(0.,0.,1.));
#28910=DIRECTION('refdir',(1.,0.,0.));
#28911=DIRECTION('center_axis',(0.,0.,1.));
#28912=DIRECTION('ref_axis',(1.,0.,0.));
#28913=DIRECTION('center_axis',(0.,0.,1.));
#28914=DIRECTION('ref_axis',(1.,0.,0.));
#28915=DIRECTION('',(0.,0.,1.));
#28916=DIRECTION('center_axis',(0.,0.,1.));
#28917=DIRECTION('ref_axis',(1.,0.,0.));
#28918=DIRECTION('center_axis',(0.,0.,1.));
#28919=DIRECTION('ref_axis',(1.,0.,0.));
#28920=DIRECTION('center_axis',(0.,0.,1.));
#28921=DIRECTION('ref_axis',(1.,0.,0.));
#28922=DIRECTION('',(0.,0.,1.));
#28923=DIRECTION('center_axis',(0.,0.,1.));
#28924=DIRECTION('ref_axis',(1.,0.,0.));
#28925=DIRECTION('center_axis',(0.,0.,1.));
#28926=DIRECTION('ref_axis',(1.,0.,0.));
#28927=DIRECTION('center_axis',(0.,0.,1.));
#28928=DIRECTION('ref_axis',(1.,0.,0.));
#28929=DIRECTION('',(0.,0.,1.));
#28930=DIRECTION('center_axis',(0.,0.,1.));
#28931=DIRECTION('ref_axis',(1.,0.,0.));
#28932=DIRECTION('center_axis',(0.,0.,1.));
#28933=DIRECTION('ref_axis',(1.,0.,0.));
#28934=DIRECTION('center_axis',(0.,0.,1.));
#28935=DIRECTION('ref_axis',(1.,0.,0.));
#28936=DIRECTION('',(0.,0.,1.));
#28937=DIRECTION('center_axis',(0.,0.,1.));
#28938=DIRECTION('ref_axis',(1.,0.,0.));
#28939=DIRECTION('center_axis',(0.,0.,1.));
#28940=DIRECTION('ref_axis',(1.,0.,0.));
#28941=DIRECTION('',(-5.33761069531325E-16,1.,0.));
#28942=DIRECTION('',(-1.,0.,0.));
#28943=DIRECTION('',(0.,1.,0.));
#28944=DIRECTION('',(-1.,0.,0.));
#28945=DIRECTION('center_axis',(-1.,0.,0.));
#28946=DIRECTION('ref_axis',(0.,0.,1.));
#28947=DIRECTION('',(0.,0.,1.));
#28948=DIRECTION('',(6.93889390390723E-16,1.,0.));
#28949=DIRECTION('',(0.,0.,-1.));
#28950=DIRECTION('',(0.,1.,0.));
#28951=DIRECTION('',(0.,0.,-1.));
#28952=DIRECTION('center_axis',(0.,-1.,0.));
#28953=DIRECTION('ref_axis',(0.,0.,-1.));
#28954=DIRECTION('',(-1.,0.,0.));
#28955=DIRECTION('',(0.,0.,1.));
#28956=DIRECTION('',(-1.,0.,0.));
#28957=DIRECTION('',(0.,0.,-1.));
#28958=DIRECTION('center_axis',(1.,0.,0.));
#28959=DIRECTION('ref_axis',(0.,0.,-1.));
#28960=DIRECTION('',(0.,-1.,0.));
#28961=DIRECTION('',(0.,0.,1.));
#28962=DIRECTION('',(0.,-1.,0.));
#28963=DIRECTION('',(0.,-1.,0.));
#28964=DIRECTION('',(0.,0.,-1.));
#28965=DIRECTION('center_axis',(0.,1.,0.));
#28966=DIRECTION('ref_axis',(0.,0.,1.));
#28967=DIRECTION('',(1.,-8.67361737988404E-17,0.));
#28968=DIRECTION('',(0.,0.,1.));
#28969=DIRECTION('',(1.,0.,0.));
#28970=DIRECTION('',(1.,0.,0.));
#28971=DIRECTION('center_axis',(0.,0.,1.));
#28972=DIRECTION('ref_axis',(1.,0.,0.));
#28973=DIRECTION('',(0.,-1.,0.));
#28974=DIRECTION('',(1.,0.,0.));
#28975=DIRECTION('center_axis',(0.,0.,1.));
#28976=DIRECTION('ref_axis',(1.,0.,0.));
#28977=DIRECTION('center_axis',(1.,5.33761069531325E-16,0.));
#28978=DIRECTION('ref_axis',(-5.33761069531325E-16,1.,0.));
#28979=DIRECTION('',(-5.33761069531325E-16,1.,0.));
#28980=DIRECTION('',(0.,0.,1.));
#28981=DIRECTION('center_axis',(0.,1.,0.));
#28982=DIRECTION('ref_axis',(0.,0.,1.));
#28983=DIRECTION('',(-1.,0.,0.));
#28984=DIRECTION('center_axis',(-1.,0.,0.));
#28985=DIRECTION('ref_axis',(0.,0.,1.));
#28986=DIRECTION('',(0.,-1.,0.));
#28987=DIRECTION('',(0.,0.,1.));
#28988=DIRECTION('center_axis',(0.,-1.,0.));
#28989=DIRECTION('ref_axis',(0.,0.,-1.));
#28990=DIRECTION('',(1.,0.,0.));
#28991=DIRECTION('center_axis',(0.,0.,1.));
#28992=DIRECTION('ref_axis',(1.,0.,0.));
#36204=CARTESIAN_POINT('',(0.,0.,0.));
#36205=CARTESIAN_POINT('Origin',(-13.5,0.5,1.));
#36206=CARTESIAN_POINT('',(-16.5,0.5,-4.));
#36207=CARTESIAN_POINT('Origin',(-13.5,0.5,-4.));
#36208=CARTESIAN_POINT('',(-16.5,0.5,1.));
#36209=CARTESIAN_POINT('',(-16.5,0.5,1.));
#36210=CARTESIAN_POINT('Origin',(-13.5,0.5,1.));
#36211=CARTESIAN_POINT('Origin',(11.5,0.5,1.));
#36212=CARTESIAN_POINT('',(8.5,0.5,-4.));
#36213=CARTESIAN_POINT('Origin',(11.5,0.5,-4.));
#36214=CARTESIAN_POINT('',(8.5,0.5,1.));
#36215=CARTESIAN_POINT('',(8.5,0.5,1.));
#36216=CARTESIAN_POINT('Origin',(11.5,0.5,1.));
#36217=CARTESIAN_POINT('Origin',(-27.,0.5,-4.));
#36218=CARTESIAN_POINT('',(-31.25,0.499999999999999,-4.));
#36219=CARTESIAN_POINT('Origin',(-27.,0.5,-4.));
#36220=CARTESIAN_POINT('',(-31.25,0.499999999999999,1.));
#36221=CARTESIAN_POINT('',(-31.25,0.499999999999999,-4.));
#36222=CARTESIAN_POINT('Origin',(-27.,0.5,1.));
#36223=CARTESIAN_POINT('Origin',(25.,0.5,-4.));
#36224=CARTESIAN_POINT('',(20.75,0.5,-4.));
#36225=CARTESIAN_POINT('Origin',(25.,0.5,-4.));
#36226=CARTESIAN_POINT('',(20.75,0.5,1.));
#36227=CARTESIAN_POINT('',(20.75,0.5,-4.));
#36228=CARTESIAN_POINT('Origin',(25.,0.5,1.));
#36229=CARTESIAN_POINT('Origin',(0.,0.,4.));
#36230=CARTESIAN_POINT('',(34.,-1.5,4.));
#36231=CARTESIAN_POINT('',(34.,11.5,4.));
#36232=CARTESIAN_POINT('',(34.,11.5,4.));
#36233=CARTESIAN_POINT('',(36.5,-1.5,4.));
#36234=CARTESIAN_POINT('',(34.,-1.5,4.));
#36235=CARTESIAN_POINT('',(36.5,11.5,4.));
#36236=CARTESIAN_POINT('',(36.5,11.5,4.));
#36237=CARTESIAN_POINT('',(-36.5,11.5,4.));
#36238=CARTESIAN_POINT('Origin',(36.5,11.5,4.));
#36239=CARTESIAN_POINT('',(36.5,-1.5,1.));
#36240=CARTESIAN_POINT('',(36.5,-1.5,1.));
#36241=CARTESIAN_POINT('',(36.5,-11.5,1.));
#36242=CARTESIAN_POINT('',(36.5,-11.5,1.));
#36243=CARTESIAN_POINT('',(36.5,-11.5,-4.));
#36244=CARTESIAN_POINT('',(36.5,-11.5,4.));
#36245=CARTESIAN_POINT('',(36.5,11.5,-4.));
#36246=CARTESIAN_POINT('',(36.5,11.5,-4.));
#36247=CARTESIAN_POINT('',(36.5,11.5,4.));
#36248=CARTESIAN_POINT('Origin',(-36.5,11.5,4.));
#36249=CARTESIAN_POINT('',(34.,11.5,1.));
#36250=CARTESIAN_POINT('',(-36.5,11.5,1.));
#36251=CARTESIAN_POINT('',(-36.5,11.5,1.));
#36252=CARTESIAN_POINT('',(34.,11.5,1.));
#36253=CARTESIAN_POINT('',(-36.5,11.5,-4.));
#36254=CARTESIAN_POINT('',(-36.5,11.5,-4.));
#36255=CARTESIAN_POINT('',(-36.5,11.5,4.));
#36256=CARTESIAN_POINT('Origin',(-36.5,11.5,4.));
#36257=CARTESIAN_POINT('',(-36.5,-9.5,4.));
#36258=CARTESIAN_POINT('',(-36.5,-11.5,4.));
#36259=CARTESIAN_POINT('',(-36.5,11.5,4.));
#36260=CARTESIAN_POINT('',(-36.5,-9.5,1.));
#36261=CARTESIAN_POINT('',(-36.5,-9.5,1.));
#36262=CARTESIAN_POINT('',(-36.5,11.5,1.));
#36263=CARTESIAN_POINT('',(-36.5,-11.5,-4.));
#36264=CARTESIAN_POINT('',(-36.5,11.5,-4.));
#36265=CARTESIAN_POINT('',(-36.5,-11.5,4.));
#36266=CARTESIAN_POINT('Origin',(-36.5,-11.5,4.));
#36267=CARTESIAN_POINT('',(16.5,-11.5,1.));
#36268=CARTESIAN_POINT('',(16.5,-11.5,1.));
#36269=CARTESIAN_POINT('',(16.5,-11.5,4.));
#36270=CARTESIAN_POINT('',(16.5,-11.5,1.));
#36271=CARTESIAN_POINT('',(-36.5,-11.5,4.));
#36272=CARTESIAN_POINT('',(-36.5,-11.5,-4.));
#36273=CARTESIAN_POINT('Origin',(0.,0.,4.));
#36274=CARTESIAN_POINT('',(16.5,-9.5,4.));
#36275=CARTESIAN_POINT('',(16.5,-9.5,4.));
#36276=CARTESIAN_POINT('',(-36.5,-9.5,4.));
#36277=CARTESIAN_POINT('Origin',(0.,0.,-4.));
#36278=CARTESIAN_POINT('Origin',(34.,11.5,1.));
#36279=CARTESIAN_POINT('',(34.,-1.5,1.));
#36280=CARTESIAN_POINT('',(34.,11.5,1.));
#36281=CARTESIAN_POINT('',(34.,-1.5,1.));
#36282=CARTESIAN_POINT('Origin',(34.,-1.5,1.));
#36283=CARTESIAN_POINT('',(34.,-1.5,1.));
#36284=CARTESIAN_POINT('Origin',(16.5,-9.5,1.));
#36285=CARTESIAN_POINT('',(16.5,-9.5,1.));
#36286=CARTESIAN_POINT('',(16.5,-9.5,1.));
#36287=CARTESIAN_POINT('',(16.5,-9.5,1.));
#36288=CARTESIAN_POINT('Origin',(-36.5,-9.5,1.));
#36289=CARTESIAN_POINT('',(-36.5,-9.5,1.));
#36290=CARTESIAN_POINT('Origin',(0.,0.,1.));
#57016=UNCERTAINTY_MEASURE_WITH_UNIT(LENGTH_MEASURE(0.01),#57080,
'DISTANCE_ACCURACY_VALUE',
'Maximum model space distance between geometric entities at asserted c
onnectivities');
#57040=UNCERTAINTY_MEASURE_WITH_UNIT(LENGTH_MEASURE(0.01),#57080,
'DISTANCE_ACCURACY_VALUE',
'Maximum model space distance between geometric entities at asserted c
onnectivities');
#57055=(
GEOMETRIC_REPRESENTATION_CONTEXT(3)
GLOBAL_UNCERTAINTY_ASSIGNED_CONTEXT((#57016))
GLOBAL_UNIT_ASSIGNED_CONTEXT((#57080,#57082,#57083))
REPRESENTATION_CONTEXT('','3D')
);
#57079=(
GEOMETRIC_REPRESENTATION_CONTEXT(3)
GLOBAL_UNCERTAINTY_ASSIGNED_CONTEXT((#57040))
GLOBAL_UNIT_ASSIGNED_CONTEXT((#57080,#57082,#57083))
REPRESENTATION_CONTEXT('','3D')
);
#57080=(
LENGTH_UNIT()
NAMED_UNIT(*)
SI_UNIT(.MILLI.,.METRE.)
);
#57082=(
NAMED_UNIT(*)
PLANE_ANGLE_UNIT()
SI_UNIT($,.RADIAN.)
);
#57083=(
NAMED_UNIT(*)
SI_UNIT($,.STERADIAN.)
SOLID_ANGLE_UNIT()
);
#57098=SHAPE_DEFINITION_REPRESENTATION(#57144,#57263);
#57144=PRODUCT_DEFINITION_SHAPE('',$,#57302);
#57263=SHAPE_REPRESENTATION('',(#25397),#57055);
#57287=PRODUCT_DEFINITION_CONTEXT('part definition',#57403,'design');
#57302=PRODUCT_DEFINITION('Ball Screw Spacer 2','Ball Screw Spacer 2',#57340,
#57287);
#57340=PRODUCT_DEFINITION_FORMATION('',$,#57419);
#57403=APPLICATION_CONTEXT(
'Core Data for Automotive Mechanical Design Process');
#57404=PRODUCT_CONTEXT('part definition',#57403,'mechanical');
#57419=PRODUCT('Ball Screw Spacer 2','Ball Screw Spacer 2',$,(#57404));
#57444=PRESENTATION_STYLE_ASSIGNMENT((#57446));
#57446=SURFACE_STYLE_USAGE(.BOTH.,#57448);
#57448=SURFACE_SIDE_STYLE('',(#57450));
#57450=SURFACE_STYLE_FILL_AREA(#57452);
#57452=FILL_AREA_STYLE('Opaque(202,209,238)',(#57454));
#57454=FILL_AREA_STYLE_COLOUR('Opaque(202,209,238)',#57456);
#57456=COLOUR_RGB('Opaque(202,209,238)',0.792156862745098,0.819607843137255,
0.933333333333333);
ENDSEC;
END-ISO-10303-21;
